ISO-10303-21;
HEADER;
/* Generated by software containing ST-Developer
 * from STEP Tools, Inc. (www.steptools.com) 
 */

FILE_DESCRIPTION(
/* description */ ('PAT-065'),
/* implementation_level */ '2;1');

FILE_NAME(
/* name */ 'Steel pad.step',
/* time_stamp */ '2026-10-28T22:09:22-07:00',
/* author */ (''),
/* organization */ (''),
/* preprocessor_version */ 'ST-DEVELOPER v20.2',
/* originating_system */ 'Autodesk Translation Framework v15.17.0.0',
/* authorisation */ '');

FILE_SCHEMA (('AUTOMOTIVE_DESIGN { 1 0 10303 214 3 1 1 }'));
ENDSEC;

DATA;
#10=MECHANICAL_DESIGN_GEOMETRIC_PRESENTATION_REPRESENTATION('',(#163),#5502);
#117=SPHERICAL_SURFACE('',#3486,0.52);
#122=CONICAL_SURFACE('',#3493,1.5,1.27933953231703);
#143=SHAPE_REPRESENTATION_RELATIONSHIP('SRR','None',#5561,#153);
#153=ADVANCED_BREP_SHAPE_REPRESENTATION('',(#173),#5497);
#163=STYLED_ITEM('',(#5680),#173);
#173=MANIFOLD_SOLID_BREP('Body1',#3210);
#191=FACE_BOUND('',#634,.T.);
#192=FACE_BOUND('',#639,.T.);
#289=PLANE('',#3482);
#290=PLANE('',#3484);
#291=PLANE('',#3489);
#292=PLANE('',#3495);
#443=FACE_OUTER_BOUND('',#631,.T.);
#444=FACE_OUTER_BOUND('',#632,.T.);
#445=FACE_OUTER_BOUND('',#633,.T.);
#446=FACE_OUTER_BOUND('',#635,.T.);
#447=FACE_OUTER_BOUND('',#636,.T.);
#448=FACE_OUTER_BOUND('',#637,.T.);
#449=FACE_OUTER_BOUND('',#638,.T.);
#631=EDGE_LOOP('',(#2722,#2723));
#632=EDGE_LOOP('',(#2724,#2725));
#633=EDGE_LOOP('',(#2726,#2727,#2728));
#634=EDGE_LOOP('',(#2729,#2730));
#635=EDGE_LOOP('',(#2731));
#636=EDGE_LOOP('',(#2732,#2733,#2734,#2735));
#637=EDGE_LOOP('',(#2736,#2737,#2738,#2739));
#638=EDGE_LOOP('',(#2740));
#639=EDGE_LOOP('',(#2741));
#952=LINE('',#5128,#1283);
#953=LINE('',#5142,#1284);
#954=LINE('',#5146,#1285);
#1283=VECTOR('',#4175,1.);
#1284=VECTOR('',#4194,2.);
#1285=VECTOR('',#4199,1.5);
#1408=CIRCLE('',#3483,0.48);
#1409=CIRCLE('',#3485,0.332264954516723);
#1410=CIRCLE('',#3487,0.48);
#1411=CIRCLE('',#3488,0.52);
#1412=CIRCLE('',#3490,2.);
#1413=CIRCLE('',#3492,2.);
#1414=CIRCLE('',#3494,1.);
#1633=VERTEX_POINT('',#5125);
#1634=VERTEX_POINT('',#5126);
#1635=VERTEX_POINT('',#5132);
#1636=VERTEX_POINT('',#5134);
#1637=VERTEX_POINT('',#5137);
#1638=VERTEX_POINT('',#5140);
#1639=VERTEX_POINT('',#5144);
#2011=EDGE_CURVE('',#1633,#1634,#1408,.T.);
#2012=EDGE_CURVE('',#1634,#1633,#952,.T.);
#2013=EDGE_CURVE('',#1634,#1633,#1409,.T.);
#2014=EDGE_CURVE('',#1635,#1635,#1410,.T.);
#2015=EDGE_CURVE('',#1636,#1635,#1411,.T.);
#2016=EDGE_CURVE('',#1637,#1637,#1412,.T.);
#2017=EDGE_CURVE('',#1638,#1638,#1413,.T.);
#2018=EDGE_CURVE('',#1638,#1637,#953,.T.);
#2019=EDGE_CURVE('',#1639,#1639,#1414,.T.);
#2020=EDGE_CURVE('',#1639,#1638,#954,.T.);
#2722=ORIENTED_EDGE('',*,*,#2011,.F.);
#2723=ORIENTED_EDGE('',*,*,#2012,.F.);
#2724=ORIENTED_EDGE('',*,*,#2013,.F.);
#2725=ORIENTED_EDGE('',*,*,#2012,.T.);
#2726=ORIENTED_EDGE('',*,*,#2014,.F.);
#2727=ORIENTED_EDGE('',*,*,#2015,.F.);
#2728=ORIENTED_EDGE('',*,*,#2015,.T.);
#2729=ORIENTED_EDGE('',*,*,#2011,.T.);
#2730=ORIENTED_EDGE('',*,*,#2013,.T.);
#2731=ORIENTED_EDGE('',*,*,#2016,.F.);
#2732=ORIENTED_EDGE('',*,*,#2017,.F.);
#2733=ORIENTED_EDGE('',*,*,#2018,.T.);
#2734=ORIENTED_EDGE('',*,*,#2016,.T.);
#2735=ORIENTED_EDGE('',*,*,#2018,.F.);
#2736=ORIENTED_EDGE('',*,*,#2019,.F.);
#2737=ORIENTED_EDGE('',*,*,#2020,.T.);
#2738=ORIENTED_EDGE('',*,*,#2017,.T.);
#2739=ORIENTED_EDGE('',*,*,#2020,.F.);
#2740=ORIENTED_EDGE('',*,*,#2019,.T.);
#2741=ORIENTED_EDGE('',*,*,#2014,.T.);
#3019=CYLINDRICAL_SURFACE('',#3491,2.);
#3137=ADVANCED_FACE('',(#443),#289,.T.);
#3138=ADVANCED_FACE('',(#444),#290,.T.);
#3139=ADVANCED_FACE('',(#445,#191),#117,.F.);
#3140=ADVANCED_FACE('',(#446),#291,.T.);
#3141=ADVANCED_FACE('',(#447),#3019,.T.);
#3142=ADVANCED_FACE('',(#448),#122,.T.);
#3143=ADVANCED_FACE('',(#449,#192),#292,.T.);
#3210=CLOSED_SHELL('',(#3137,#3138,#3139,#3140,#3141,#3142,#3143));
#3481=AXIS2_PLACEMENT_3D('',#5123,#4169,#4170);
#3482=AXIS2_PLACEMENT_3D('',#5124,#4171,#4172);
#3483=AXIS2_PLACEMENT_3D('',#5127,#4173,#4174);
#3484=AXIS2_PLACEMENT_3D('',#5129,#4176,#4177);
#3485=AXIS2_PLACEMENT_3D('',#5130,#4178,#4179);
#3486=AXIS2_PLACEMENT_3D('',#5131,#4180,#4181);
#3487=AXIS2_PLACEMENT_3D('',#5133,#4182,#4183);
#3488=AXIS2_PLACEMENT_3D('',#5135,#4184,#4185);
#3489=AXIS2_PLACEMENT_3D('',#5136,#4186,#4187);
#3490=AXIS2_PLACEMENT_3D('',#5138,#4188,#4189);
#3491=AXIS2_PLACEMENT_3D('',#5139,#4190,#4191);
#3492=AXIS2_PLACEMENT_3D('',#5141,#4192,#4193);
#3493=AXIS2_PLACEMENT_3D('',#5143,#4195,#4196);
#3494=AXIS2_PLACEMENT_3D('',#5145,#4197,#4198);
#3495=AXIS2_PLACEMENT_3D('',#5147,#4200,#4201);
#4169=DIRECTION('axis',(0.,0.,1.));
#4170=DIRECTION('refdir',(1.,0.,0.));
#4171=DIRECTION('center_axis',(0.,-1.,0.));
#4172=DIRECTION('ref_axis',(1.,0.,0.));
#4173=DIRECTION('center_axis',(0.,1.,0.));
#4174=DIRECTION('ref_axis',(0.,0.,1.));
#4175=DIRECTION('',(1.,0.,0.));
#4176=DIRECTION('center_axis',(0.,0.,1.));
#4177=DIRECTION('ref_axis',(1.,0.,0.));
#4178=DIRECTION('center_axis',(0.,0.,-1.));
#4179=DIRECTION('ref_axis',(0.,1.,0.));
#4180=DIRECTION('center_axis',(6.12323399573676E-17,0.,1.));
#4181=DIRECTION('ref_axis',(1.,0.,0.));
#4182=DIRECTION('center_axis',(0.,0.,-1.));
#4183=DIRECTION('ref_axis',(0.,1.,0.));
#4184=DIRECTION('center_axis',(-1.22464679914735E-16,1.,0.));
#4185=DIRECTION('ref_axis',(-1.,-1.22464679914735E-16,0.));
#4186=DIRECTION('center_axis',(0.,0.,-1.));
#4187=DIRECTION('ref_axis',(-1.,0.,0.));
#4188=DIRECTION('center_axis',(0.,0.,1.));
#4189=DIRECTION('ref_axis',(1.,0.,0.));
#4190=DIRECTION('center_axis',(0.,0.,1.));
#4191=DIRECTION('ref_axis',(1.,0.,0.));
#4192=DIRECTION('center_axis',(0.,0.,1.));
#4193=DIRECTION('ref_axis',(1.,0.,0.));
#4194=DIRECTION('',(0.,0.,-1.));
#4195=DIRECTION('center_axis',(0.,0.,-1.));
#4196=DIRECTION('ref_axis',(1.,0.,0.));
#4197=DIRECTION('center_axis',(0.,0.,1.));
#4198=DIRECTION('ref_axis',(1.,0.,0.));
#4199=DIRECTION('',(-0.957826285221151,-1.17299889433528E-16,-0.287347885566345));
#4200=DIRECTION('center_axis',(0.,0.,1.));
#4201=DIRECTION('ref_axis',(1.,0.,0.));
#5123=CARTESIAN_POINT('',(0.,0.,0.));
#5124=CARTESIAN_POINT('Origin',(-0.3,0.2,0.4));
#5125=CARTESIAN_POINT('',(0.265329983228433,0.2,0.7));
#5126=CARTESIAN_POINT('',(-0.265329983228432,0.2,0.7));
#5127=CARTESIAN_POINT('Origin',(1.11022302462516E-16,0.2,1.1));
#5128=CARTESIAN_POINT('',(-0.3,0.2,0.7));
#5129=CARTESIAN_POINT('Origin',(0.,0.4,0.7));
#5130=CARTESIAN_POINT('Origin',(1.11022302462516E-16,0.,0.7));
#5131=CARTESIAN_POINT('Origin',(1.11022302462516E-16,0.,1.1));
#5132=CARTESIAN_POINT('',(-0.48,-5.8783046359073E-17,1.3));
#5133=CARTESIAN_POINT('Origin',(1.11022302462516E-16,0.,1.3));
#5134=CARTESIAN_POINT('',(7.91814856846845E-17,-3.89937543492083E-33,0.58));
#5135=CARTESIAN_POINT('Origin',(1.11022302462516E-16,0.,1.1));
#5136=CARTESIAN_POINT('Origin',(2.,0.,0.4));
#5137=CARTESIAN_POINT('',(-2.,-2.44929359829471E-16,0.4));
#5138=CARTESIAN_POINT('Origin',(0.,0.,0.4));
#5139=CARTESIAN_POINT('Origin',(0.,0.,0.7));
#5140=CARTESIAN_POINT('',(-2.,-2.44929359829471E-16,1.));
#5141=CARTESIAN_POINT('Origin',(0.,0.,1.));
#5142=CARTESIAN_POINT('',(-2.,-2.44929359829471E-16,0.7));
#5143=CARTESIAN_POINT('Origin',(0.,0.,1.15));
#5144=CARTESIAN_POINT('',(-1.,-1.22464679914735E-16,1.3));
#5145=CARTESIAN_POINT('Origin',(0.,0.,1.3));
#5146=CARTESIAN_POINT('',(-1.5,-1.83697019872103E-16,1.15));
#5147=CARTESIAN_POINT('Origin',(0.,0.,1.3));
#5484=UNCERTAINTY_MEASURE_WITH_UNIT(LENGTH_MEASURE(0.001),#5503,
'DISTANCE_ACCURACY_VALUE',
'Maximum model space distance between geometric entities at asserted c
onnectivities');
#5489=UNCERTAINTY_MEASURE_WITH_UNIT(LENGTH_MEASURE(0.001),#5503,
'DISTANCE_ACCURACY_VALUE',
'Maximum model space distance between geometric entities at asserted c
onnectivities');
#5497=(
GEOMETRIC_REPRESENTATION_CONTEXT(3)
GLOBAL_UNCERTAINTY_ASSIGNED_CONTEXT((#5484))
GLOBAL_UNIT_ASSIGNED_CONTEXT((#5503,#5505,#5506))
REPRESENTATION_CONTEXT('','3D')
);
#5502=(
GEOMETRIC_REPRESENTATION_CONTEXT(3)
GLOBAL_UNCERTAINTY_ASSIGNED_CONTEXT((#5489))
GLOBAL_UNIT_ASSIGNED_CONTEXT((#5503,#5505,#5506))
REPRESENTATION_CONTEXT('','3D')
);
#5503=(
LENGTH_UNIT()
NAMED_UNIT(*)
SI_UNIT(.CENTI.,.METRE.)
);
#5505=(
NAMED_UNIT(*)
PLANE_ANGLE_UNIT()
SI_UNIT($,.RADIAN.)
);
#5506=(
NAMED_UNIT(*)
SI_UNIT($,.STERADIAN.)
SOLID_ANGLE_UNIT()
);
#5514=SHAPE_DEFINITION_REPRESENTATION(#5526,#5561);
#5526=PRODUCT_DEFINITION_SHAPE('',$,#5574);
#5561=SHAPE_REPRESENTATION('',(#3481),#5497);
#5566=PRODUCT_DEFINITION_CONTEXT('part definition',#5604,'design');
#5574=PRODUCT_DEFINITION('Steel pad','Steel pad',#5586,
#5566);
#5586=PRODUCT_DEFINITION_FORMATION('',$,#5613);
#5604=APPLICATION_CONTEXT(
'Core Data for Automotive Mechanical Design Process');
#5605=PRODUCT_CONTEXT('part definition',#5604,'mechanical');
#5613=PRODUCT('Steel pad','Steel pad','Steel pad',(#5605));
#5674=COLOUR_RGB('Light Blue',0.38,0.62,0.78);
#5675=FILL_AREA_STYLE_COLOUR('',#5674);
#5676=FILL_AREA_STYLE('',(#5675));
#5677=SURFACE_STYLE_FILL_AREA(#5676);
#5678=SURFACE_SIDE_STYLE('',(#5677));
#5679=SURFACE_STYLE_USAGE(.BOTH.,#5678);
#5680=PRESENTATION_STYLE_ASSIGNMENT((#5679));
ENDSEC;
END-ISO-10303-21;
